ISO-10303-21;
HEADER;
FILE_DESCRIPTION (('STEP AP214'),
    '1' );
FILE_NAME ('socket head cap screw_iso_ISO 4762 M4 x 8 - 8N.step',
    '2026-10-08T05:45:04',
    ( '' ),
    ( '' ),
    'SwSTEP 2.0',
    'SolidWorks 2026',
    '' );
FILE_SCHEMA (( 'AUTOMOTIVE_DESIGN' ));
ENDSEC;

DATA;
#11=FACE_OUTER_BOUND ( 'NONE', #1428, .T. ) ;
#28=ORIENTED_EDGE ( 'NONE', *, *, #6003, .T. ) ;
#83=CIRCLE ( 'NONE', #1502, 3.500000000000000000 ) ;
#103=CARTESIAN_POINT ( 'NONE',  ( 4.200000000000001954, 0.000000000000000000, 0.000000000000000000 ) ) ;
#110=CARTESIAN_POINT ( 'NONE',  ( 4.200000000000001954, 0.000000000000000000, 2.000000000000000888 ) ) ;
#120=EDGE_CURVE ( 'NONE', #1703, #4005, #3527, .T. ) ;
#134=CONICAL_SURFACE ( 'NONE', #6343, 1.610000000000000098, 0.7853981633974741472 ) ;
#146=ADVANCED_FACE ( 'NONE', ( #1748 ), #9290, .T. ) ;
#155=EDGE_LOOP ( 'NONE', ( #5166, #1454, #3473, #6221, #8889 ) ) ;
#174=ORIENTED_EDGE ( 'NONE', *, *, #8829, .T. ) ;
#182=DIRECTION ( 'NONE',  ( 0.000000000000000000, -1.000000000000000000, 9.783878858594328898E-16 ) ) ;
#185=FACE_OUTER_BOUND ( 'NONE', #10123, .T. ) ;
#194=FACE_OUTER_BOUND ( 'NONE', #2327, .T. ) ;
#206=CARTESIAN_POINT ( 'NONE',  ( 2.000000000000000000, 0.000000000000000000, 0.000000000000000000 ) ) ;
#210=DIRECTION ( 'NONE',  ( 0.000000000000000000, 1.000000000000000000, -1.345283343056720273E-15 ) ) ;
#216=ORIENTED_EDGE ( 'NONE', *, *, #9478, .T. ) ;
#222=ORIENTED_EDGE ( 'NONE', *, *, #1600, .T. ) ;
#227=ADVANCED_FACE ( 'NONE', ( #1969 ), #10407, .F. ) ;
#233=VERTEX_POINT ( 'NONE', #9571 ) ;
#246=AXIS2_PLACEMENT_3D ( 'NONE', #4153, #7547, #5055 ) ;
#248=DIRECTION ( 'NONE',  ( 0.000000000000000000, 0.000000000000000000, -1.000000000000000000 ) ) ;
#266=DIRECTION ( 'NONE',  ( 0.000000000000000000, 0.8660254037844380415, -0.5000000000000012212 ) ) ;
#282=ADVANCED_FACE ( 'NONE', ( #10574 ), #1338, .F. ) ;
#291=ADVANCED_FACE ( 'NONE', ( #6283 ), #7022, .T. ) ;
#296=PLANE ( 'NONE',  #4705 ) ;
#299=CARTESIAN_POINT ( 'NONE',  ( 2.000000000000000000, 0.8865213383406715941, 1.535499999999999199 ) ) ;
#308=AXIS2_PLACEMENT_3D ( 'NONE', #6956, #4296, #9565 ) ;
#340=CARTESIAN_POINT ( 'NONE',  ( 2.000000000000000000, 1.773042676681340524, -2.059984127722458425E-15 ) ) ;
#352=CARTESIAN_POINT ( 'NONE',  ( 0.1999999999999987899, 0.000000000000000000, 3.500000000000000000 ) ) ;
#359=FACE_OUTER_BOUND ( 'NONE', #4823, .T. ) ;
#368=DIRECTION ( 'NONE',  ( 0.000000000000000000, 0.000000000000000000, -1.000000000000000000 ) ) ;
#376=ORIENTED_EDGE ( 'NONE', *, *, #1216, .F. ) ;
#386=CARTESIAN_POINT ( 'NONE',  ( 4.000000000000000000, 0.000000000000000000, 0.000000000000000000 ) ) ;
#390=DIRECTION ( 'NONE',  ( 1.000000000000000000, 0.000000000000000000, 0.000000000000000000 ) ) ;
#411=CARTESIAN_POINT ( 'NONE',  ( 4.000000000000003553, 0.000000000000000000, 3.500000000000000000 ) ) ;
#423=DIRECTION ( 'NONE',  ( 1.000000000000000000, 0.000000000000000000, 0.000000000000000000 ) ) ;
#426=AXIS2_PLACEMENT_3D ( 'NONE', #206, #8665, #6156 ) ;
#440=ADVANCED_FACE ( 'NONE', ( #7446 ), #6442, .F. ) ;
#444=VECTOR ( 'NONE', #10181, 1000.000000000000000 ) ;
#449=EDGE_LOOP ( 'NONE', ( #1165, #1039, #7351, #5920, #1589 ) ) ;
#472=LINE ( 'NONE', #3971, #9797 ) ;
#477=DIRECTION ( 'NONE',  ( -1.000000000000000000, -0.000000000000000000, -0.000000000000000000 ) ) ;
#479=EDGE_LOOP ( 'NONE', ( #4396, #7220, #4636, #9662 ) ) ;
#496=AXIS2_PLACEMENT_3D ( 'NONE', #9924, #9081, #4871 ) ;
#526=LINE ( 'NONE', #9765, #6655 ) ;
#535=ORIENTED_EDGE ( 'NONE', *, *, #3962, .F. ) ;
#539=ORIENTED_EDGE ( 'NONE', *, *, #3211, .F. ) ;
#549=CARTESIAN_POINT ( 'NONE',  ( 2.000000000000000000, 1.773042676681340524, -2.059984127722458425E-15 ) ) ;
#621=ORIENTED_EDGE ( 'NONE', *, *, #5333, .T. ) ;
#630=DIRECTION ( 'NONE',  ( -1.000000000000000000, -0.000000000000000000, -0.000000000000000000 ) ) ;
#635=EDGE_CURVE ( 'NONE', #1703, #7385, #9558, .T. ) ;
#641=CARTESIAN_POINT ( 'NONE',  ( 2.000000000000000000, 1.329782007511004727, -0.7677500000000018199 ) ) ;
#664=DIRECTION ( 'NONE',  ( 1.000000000000000000, 0.000000000000000000, 0.000000000000000000 ) ) ;
#699=ORIENTED_EDGE ( 'NONE', *, *, #1713, .T. ) ;
#705=ORIENTED_EDGE ( 'NONE', *, *, #5043, .F. ) ;
#715=ORIENTED_EDGE ( 'NONE', *, *, #7861, .T. ) ;
#722=CARTESIAN_POINT ( 'NONE',  ( 2.000000000000000000, 0.8865213383406680414, -1.535500000000000975 ) ) ;
#737=CARTESIAN_POINT ( 'NONE',  ( 0.1999999999999987899, 0.000000000000000000, 0.000000000000000000 ) ) ;
#743=EDGE_CURVE ( 'NONE', #932, #3081, #7495, .T. ) ;
#744=DIRECTION ( 'NONE',  ( 0.000000000000000000, -0.5000000000000011102, -0.8660254037844379305 ) ) ;
#759=PLANE ( 'NONE',  #6344 ) ;
#762=AXIS2_PLACEMENT_3D ( 'NONE', #3197, #8099, #3823 ) ;
#872=ORIENTED_EDGE ( 'NONE', *, *, #9755, .T. ) ;
#875=CARTESIAN_POINT ( 'NONE',  ( 2.000000000000000000, 0.000000000000000000, 1.535500000000000087 ) ) ;
#919=ADVANCED_FACE ( 'NONE', ( #10227 ), #3228, .T. ) ;
#922=DIRECTION ( 'NONE',  ( 0.000000000000000000, 0.4999999999999989453, -0.8660254037844391517 ) ) ;
#927=VERTEX_POINT ( 'NONE', #110 ) ;
#930=CARTESIAN_POINT ( 'NONE',  ( 11.99999999999999645, 0.000000000000000000, 1.610000000000000098 ) ) ;
#932=VERTEX_POINT ( 'NONE', #6897 ) ;
#940=CARTESIAN_POINT ( 'NONE',  ( 11.99999999999999645, 0.000000000000000000, 0.000000000000000000 ) ) ;
#977=AXIS2_PLACEMENT_3D ( 'NONE', #103, #1834, #2727 ) ;
#982=VECTOR ( 'NONE', #2400, 1000.000000000000000 ) ;
#989=CARTESIAN_POINT ( 'NONE',  ( 4.200000000000001954, 2.449293598294707893E-16, -2.000000000000000888 ) ) ;
#1039=ORIENTED_EDGE ( 'NONE', *, *, #1517, .F. ) ;
#1045=ORIENTED_EDGE ( 'NONE', *, *, #7098, .T. ) ;
#1065=DIRECTION ( 'NONE',  ( -0.000000000000000000, 0.000000000000000000, 1.000000000000000000 ) ) ;
#1072=SURFACE_STYLE_FILL_AREA ( #8696 ) ;
#1084=UNCERTAINTY_MEASURE_WITH_UNIT (LENGTH_MEASURE( 1.000000000000000082E-05 ), #3943, 'distance_accuracy_value', 'NONE');
#1095=CARTESIAN_POINT ( 'NONE',  ( 2.000000000000000000, -1.329782007511005837, 0.7677500000000023750 ) ) ;
#1103=DIRECTION ( 'NONE',  ( 0.000000000000000000, 0.000000000000000000, 1.000000000000000000 ) ) ;
#1138=CARTESIAN_POINT ( 'NONE',  ( 0.1999999999999987899, 0.000000000000000000, 0.000000000000000000 ) ) ;
#1139=LINE ( 'NONE', #9759, #4350 ) ;
#1165=ORIENTED_EDGE ( 'NONE', *, *, #10968, .F. ) ;
#1171=CARTESIAN_POINT ( 'NONE',  ( 2.000000000000000000, 0.8865213383406715941, 1.535499999999999199 ) ) ;
#1191=FACE_OUTER_BOUND ( 'NONE', #4449, .T. ) ;
#1197=CIRCLE ( 'NONE', #1736, 3.500000000000000000 ) ;
#1199=DIRECTION ( 'NONE',  ( -1.000000000000000000, -0.000000000000000000, -0.000000000000000000 ) ) ;
#1203=DIRECTION ( 'NONE',  ( 0.000000000000000000, 0.000000000000000000, 1.000000000000000000 ) ) ;
#1216=EDGE_CURVE ( 'NONE', #3863, #7385, #8026, .T. ) ;
#1223=SHAPE_REPRESENTATION ( 'socket head cap screw_iso_ISO 4762 M4 x 8 - 8N', ( #308 ), #7601 ) ;
#1249=CARTESIAN_POINT ( 'NONE',  ( 0.000000000000000000, -0.8865213383406694847, 1.535500000000001419 ) ) ;
#1266=CARTESIAN_POINT ( 'NONE',  ( 2.000000000000000000, 0.000000000000000000, 0.000000000000000000 ) ) ;
#1272=EDGE_CURVE ( 'NONE', #10716, #3226, #5436, .T. ) ;
#1279=ORIENTED_EDGE ( 'NONE', *, *, #10345, .F. ) ;
#1338=CONICAL_SURFACE ( 'NONE', #2226, 1.535500000000000087, 1.047197551196590748 ) ;
#1348=CIRCLE ( 'NONE', #7555, 1.535500000000000087 ) ;
#1356=LINE ( 'NONE', #3027, #982 ) ;
#1378=DIRECTION ( 'NONE',  ( 0.000000000000000000, 0.000000000000000000, 1.000000000000000000 ) ) ;
#1393=EDGE_CURVE ( 'NONE', #9720, #9782, #10519, .T. ) ;
#1405=CARTESIAN_POINT ( 'NONE',  ( 2.000000000000000000, 1.773042676681340524, -2.059984127722458425E-15 ) ) ;
#1406=VERTEX_POINT ( 'NONE', #4609 ) ;
#1407=ORIENTED_EDGE ( 'NONE', *, *, #120, .T. ) ;
#1428=EDGE_LOOP ( 'NONE', ( #3496, #8625, #535, #6616 ) ) ;
#1440=DIRECTION ( 'NONE',  ( 0.000000000000000000, 0.000000000000000000, -1.000000000000000000 ) ) ;
#1454=ORIENTED_EDGE ( 'NONE', *, *, #120, .F. ) ;
#1487=VERTEX_POINT ( 'NONE', #7258 ) ;
#1495=( NAMED_UNIT ( * ) SI_UNIT ( $, .STERADIAN. ) SOLID_ANGLE_UNIT ( ) );
#1502=AXIS2_PLACEMENT_3D ( 'NONE', #5432, #7146, #10434 ) ;
#1505=ORIENTED_EDGE ( 'NONE', *, *, #5333, .F. ) ;
#1517=EDGE_CURVE ( 'NONE', #233, #4272, #4770, .T. ) ;
#1533=EDGE_CURVE ( 'NONE', #2047, #9268, #472, .T. ) ;
#1564=AXIS2_PLACEMENT_3D ( 'NONE', #8387, #2187, #5889 ) ;
#1569=FACE_OUTER_BOUND ( 'NONE', #3007, .T. ) ;
#1574=DIRECTION ( 'NONE',  ( -1.000000000000000000, -0.000000000000000000, -0.000000000000000000 ) ) ;
#1589=ORIENTED_EDGE ( 'NONE', *, *, #9537, .T. ) ;
#1590=ADVANCED_FACE ( 'NONE', ( #6521 ), #5132, .F. ) ;
#1600=EDGE_CURVE ( 'NONE', #4884, #5586, #8535, .T. ) ;
#1604=CARTESIAN_POINT ( 'NONE',  ( 2.000000000000000000, -1.773042676681341856, 2.276824562219559311E-15 ) ) ;
#1609=( NAMED_UNIT ( * ) SI_UNIT ( $, .STERADIAN. ) SOLID_ANGLE_UNIT ( ) );
#1624=EDGE_CURVE ( 'NONE', #3081, #932, #7240, .T. ) ;
#1681=STYLED_ITEM ( 'NONE', ( #3272 ), #9072 ) ;
#1685=CARTESIAN_POINT ( 'NONE',  ( -31.74999999999995737, 0.000000000000000000, 0.000000000000000000 ) ) ;
#1699=CARTESIAN_POINT ( 'NONE',  ( 2.000000000000000000, -1.773042676681341856, 2.276824562219559311E-15 ) ) ;
#1703=VERTEX_POINT ( 'NONE', #4984 ) ;
#1706=CARTESIAN_POINT ( 'NONE',  ( 2.000000000000000000, -0.8865213383406694847, 1.535500000000001419 ) ) ;
#1713=EDGE_CURVE ( 'NONE', #3725, #4079, #1758, .T. ) ;
#1715=VERTEX_POINT ( 'NONE', #10980 ) ;
#1724=CARTESIAN_POINT ( 'NONE',  ( 2.000000000000000000, -0.8865213383406694847, 1.535500000000001419 ) ) ;
#1736=AXIS2_PLACEMENT_3D ( 'NONE', #10463, #5458, #8733 ) ;
#1748=FACE_OUTER_BOUND ( 'NONE', #10082, .T. ) ;
#1756=( GEOMETRIC_REPRESENTATION_CONTEXT ( 3 ) GLOBAL_UNCERTAINTY_ASSIGNED_CONTEXT ( ( #10432 ) ) GLOBAL_UNIT_ASSIGNED_CONTEXT ( ( #7554, #3333, #1495 ) ) REPRESENTATION_CONTEXT ( 'NONE', 'WORKASPACE' ) );
#1758=CIRCLE ( 'NONE', #4421, 3.500000000000000000 ) ;
#1771=CARTESIAN_POINT ( 'NONE',  ( 0.000000000000000000, -1.773042676681341856, 2.276824562219559311E-15 ) ) ;
#1807=ADVANCED_FACE ( 'NONE', ( #10422 ), #2983, .F. ) ;
#1829=CARTESIAN_POINT ( 'NONE',  ( 0.1999999999999987899, 0.000000000000000000, 3.299999999999999822 ) ) ;
#1834=DIRECTION ( 'NONE',  ( 1.000000000000000000, 0.000000000000000000, 0.000000000000000000 ) ) ;
#1880=ADVANCED_FACE ( 'NONE', ( #10685 ), #2459, .T. ) ;
#1899=DIRECTION ( 'NONE',  ( -1.000000000000000000, -0.000000000000000000, -0.000000000000000000 ) ) ;
#1907=VERTEX_POINT ( 'NONE', #2450 ) ;
#1969=FACE_OUTER_BOUND ( 'NONE', #4251, .T. ) ;
#1975=DIRECTION ( 'NONE',  ( 1.000000000000000000, 0.000000000000000000, 0.000000000000000000 ) ) ;
#1980=DIRECTION ( 'NONE',  ( 0.000000000000000000, 1.224646799147353207E-16, 1.000000000000000000 ) ) ;
#2007=ORIENTED_EDGE ( 'NONE', *, *, #10625, .F. ) ;
#2036=VECTOR ( 'NONE', #630, 1000.000000000000000 ) ;
#2042=DIRECTION ( 'NONE',  ( -0.5000000000000061062, 1.060575238724902601E-16, -0.8660254037844351549 ) ) ;
#2047=VERTEX_POINT ( 'NONE', #4641 ) ;
#2063=ORIENTED_EDGE ( 'NONE', *, *, #10758, .T. ) ;
#2119=ORIENTED_EDGE ( 'NONE', *, *, #8304, .T. ) ;
#2157=ORIENTED_EDGE ( 'NONE', *, *, #3221, .F. ) ;
#2170=ORIENTED_EDGE ( 'NONE', *, *, #9755, .F. ) ;
#2187=DIRECTION ( 'NONE',  ( -1.000000000000000000, -0.000000000000000000, -0.000000000000000000 ) ) ;
#2208=ORIENTED_EDGE ( 'NONE', *, *, #6301, .T. ) ;
#2226=AXIS2_PLACEMENT_3D ( 'NONE', #2807, #8064, #5464 ) ;
#2235=AXIS2_PLACEMENT_3D ( 'NONE', #3485, #10364, #1980 ) ;
#2254=EDGE_CURVE ( 'NONE', #3863, #10456, #6609, .T. ) ;
#2263=VECTOR ( 'NONE', #8699, 1000.000000000000114 ) ;
#2313=ORIENTED_EDGE ( 'NONE', *, *, #7841, .T. ) ;
#2327=EDGE_LOOP ( 'NONE', ( #2350, #6094, #6510, #2535 ) ) ;
#2330=SURFACE_STYLE_FILL_AREA ( #6654 ) ;
#2333=ADVANCED_FACE ( 'NONE', ( #5737 ), #7456, .F. ) ;
#2345=AXIS2_PLACEMENT_3D ( 'NONE', #2543, #10988, #8425 ) ;
#2350=ORIENTED_EDGE ( 'NONE', *, *, #8304, .F. ) ;
#2399=AXIS2_PLACEMENT_3D ( 'NONE', #7239, #8226, #3126 ) ;
#2400=DIRECTION ( 'NONE',  ( -1.000000000000000000, -0.000000000000000000, -0.000000000000000000 ) ) ;
#2437=EDGE_LOOP ( 'NONE', ( #7777, #6794 ) ) ;
#2442=ORIENTED_EDGE ( 'NONE', *, *, #1216, .T. ) ;
#2448=CARTESIAN_POINT ( 'NONE',  ( 12.00000000000000000, 1.610000000000000098, 0.000000000000000000 ) ) ;
#2450=CARTESIAN_POINT ( 'NONE',  ( 11.61000000000001542, 0.000000000000000000, 2.000000000000000888 ) ) ;
#2459=TOROIDAL_SURFACE ( 'NONE', #1564, 3.299999999999999822, 0.2000000000000000111 ) ;
#2500=DIRECTION ( 'NONE',  ( -0.000000000000000000, 1.345283343056720273E-15, 1.000000000000000000 ) ) ;
#2520=EDGE_LOOP ( 'NONE', ( #5629, #8214, #10726, #5978 ) ) ;
#2535=ORIENTED_EDGE ( 'NONE', *, *, #6003, .F. ) ;
#2537=CARTESIAN_POINT ( 'NONE',  ( 11.61000000000001542, 2.449293598294707893E-16, -2.000000000000000888 ) ) ;
#2543=CARTESIAN_POINT ( 'NONE',  ( 2.000000000000000000, 0.000000000000000000, 0.000000000000000000 ) ) ;
#2545=ORIENTED_EDGE ( 'NONE', *, *, #2925, .F. ) ;
#2575=CARTESIAN_POINT ( 'NONE',  ( 0.000000000000000000, 1.773042676681340524, -2.059984127722458425E-15 ) ) ;
#2583=FACE_BOUND ( 'NONE', #10774, .T. ) ;
#2610=EDGE_LOOP ( 'NONE', ( #6270, #5692, #6112 ) ) ;
#2621=PLANE ( 'NONE',  #10776 ) ;
#2632=AXIS2_PLACEMENT_3D ( 'NONE', #4250, #7750, #1065 ) ;
#2660=CARTESIAN_POINT ( 'NONE',  ( 2.000000000000000000, -1.773042676681341856, 2.276824562219559311E-15 ) ) ;
#2682=CARTESIAN_POINT ( 'NONE',  ( 11.99999999999999645, 0.000000000000000000, 1.610000000000000098 ) ) ;
#2711=CARTESIAN_POINT ( 'NONE',  ( 4.200000000000001954, 0.000000000000000000, 0.000000000000000000 ) ) ;
#2727=DIRECTION ( 'NONE',  ( 0.000000000000000000, 0.000000000000000000, -1.000000000000000000 ) ) ;
#2735=EDGE_LOOP ( 'NONE', ( #10556, #4511, #5328, #222, #174 ) ) ;
#2742=DIRECTION ( 'NONE',  ( -1.000000000000000000, -0.000000000000000000, -0.000000000000000000 ) ) ;
#2767=AXIS2_PLACEMENT_3D ( 'NONE', #340, #390, #4687 ) ;
#2782=CARTESIAN_POINT ( 'NONE',  ( 11.99999999999999645, 0.000000000000000000, 0.000000000000000000 ) ) ;
#2797=ORIENTED_EDGE ( 'NONE', *, *, #10906, .F. ) ;
#2807=CARTESIAN_POINT ( 'NONE',  ( 2.000000000000000000, 0.000000000000000000, 0.000000000000000000 ) ) ;
#2861=CARTESIAN_POINT ( 'NONE',  ( 2.000000000000000000, -0.8865213383406694847, 1.535500000000001419 ) ) ;
#2864=DIRECTION ( 'NONE',  ( 1.000000000000000000, 0.000000000000000000, 0.000000000000000000 ) ) ;
#2888=APPLICATION_CONTEXT ( 'automotive_design' ) ;
#2890=DIRECTION ( 'NONE',  ( 0.000000000000000000, 0.000000000000000000, 1.000000000000000000 ) ) ;
#2912=CARTESIAN_POINT ( 'NONE',  ( -31.74999999999995737, 4.286263797015736595E-16, -3.500000000000000000 ) ) ;
#2919=CARTESIAN_POINT ( 'NONE',  ( 2.000000000000000000, 1.773042676681340524, -2.059984127722458425E-15 ) ) ;
#2925=EDGE_CURVE ( 'NONE', #5562, #4884, #4971, .T. ) ;
#2960=CIRCLE ( 'NONE', #3666, 2.000000000000000888 ) ;
#2983=PLANE ( 'NONE',  #9729 ) ;
#2993=DIRECTION ( 'NONE',  ( 1.000000000000000000, 0.000000000000000000, 0.000000000000000000 ) ) ;
#3001=VECTOR ( 'NONE', #6082, 1000.000000000000227 ) ;
#3007=EDGE_LOOP ( 'NONE', ( #7531, #9665, #9846, #2007, #8858 ) ) ;
#3018=CARTESIAN_POINT ( 'NONE',  ( 11.99999999999999645, 2.210487472460973191E-16, -1.610000000000000098 ) ) ;
#3027=CARTESIAN_POINT ( 'NONE',  ( 2.000000000000000000, 0.8865213383406680414, -1.535500000000000975 ) ) ;
#3032=CYLINDRICAL_SURFACE ( 'NONE', #7369, 2.000000000000000888 ) ;
#3039=CARTESIAN_POINT ( 'NONE',  ( 2.000000000000000000, -0.8865213383406694847, 1.535500000000001419 ) ) ;
#3048=FACE_OUTER_BOUND ( 'NONE', #2520, .T. ) ;
#3081=VERTEX_POINT ( 'NONE', #5219 ) ;
#3096=CARTESIAN_POINT ( 'NONE',  ( 2.000000000000000000, 1.773042676681340524, -2.059984127722458425E-15 ) ) ;
#3101=MECHANICAL_DESIGN_GEOMETRIC_PRESENTATION_REPRESENTATION('',(#1681),#6638);
#3104=CIRCLE ( 'NONE', #977, 2.000000000000000888 ) ;
#3126=DIRECTION ( 'NONE',  ( 0.000000000000000000, 0.000000000000000000, 1.000000000000000000 ) ) ;
#3130=CARTESIAN_POINT ( 'NONE',  ( -31.74999999999995737, 0.000000000000000000, 2.000000000000000888 ) ) ;
#3197=CARTESIAN_POINT ( 'NONE',  ( 11.99999999999999645, 0.000000000000000000, 0.000000000000000000 ) ) ;
#3211=EDGE_CURVE ( 'NONE', #3226, #4884, #4545, .T. ) ;
#3215=ORIENTED_EDGE ( 'NONE', *, *, #7423, .F. ) ;
#3221=EDGE_CURVE ( 'NONE', #4005, #2047, #526, .T. ) ;
#3226=VERTEX_POINT ( 'NONE', #3972 ) ;
#3228=CONICAL_SURFACE ( 'NONE', #6068, 1.610000000000000098, 0.7853981633974741472 ) ;
#3242=ORIENTED_EDGE ( 'NONE', *, *, #9626, .F. ) ;
#3268=ORIENTED_EDGE ( 'NONE', *, *, #1600, .F. ) ;
#3272=PRESENTATION_STYLE_ASSIGNMENT (( #10416 ) ) ;
#3315=LINE ( 'NONE', #1706, #4601 ) ;
#3333=( NAMED_UNIT ( * ) PLANE_ANGLE_UNIT ( ) SI_UNIT ( $, .RADIAN. ) );
#3335=FACE_OUTER_BOUND ( 'NONE', #5989, .T. ) ;
#3347=ORIENTED_EDGE ( 'NONE', *, *, #7703, .T. ) ;
#3377=CARTESIAN_POINT ( 'NONE',  ( 2.000000000000000000, -1.773042676681341856, 2.276824562219559311E-15 ) ) ;
#3391=FACE_OUTER_BOUND ( 'NONE', #5056, .T. ) ;
#3419=VECTOR ( 'NONE', #8149, 1000.000000000000000 ) ;
#3471=DIRECTION ( 'NONE',  ( -1.000000000000000000, -0.000000000000000000, -0.000000000000000000 ) ) ;
#3473=ORIENTED_EDGE ( 'NONE', *, *, #8406, .T. ) ;
#3485=CARTESIAN_POINT ( 'NONE',  ( 4.200000000000001954, 2.694222958124178486E-16, 2.200000000000001066 ) ) ;
#3487=VECTOR ( 'NONE', #8740, 1000.000000000000114 ) ;
#3496=ORIENTED_EDGE ( 'NONE', *, *, #7423, .T. ) ;
#3519=EDGE_CURVE ( 'NONE', #927, #1487, #10573, .T. ) ;
#3527=LINE ( 'NONE', #7576, #7903 ) ;
#3552=EDGE_CURVE ( 'NONE', #4884, #7995, #1348, .T. ) ;
#3570=ORIENTED_EDGE ( 'NONE', *, *, #10590, .T. ) ;
#3584=PLANE ( 'NONE',  #8096 ) ;
#3593=ORIENTED_EDGE ( 'NONE', *, *, #635, .T. ) ;
#3604=ORIENTED_EDGE ( 'NONE', *, *, #1272, .T. ) ;
#3607=DIRECTION ( 'NONE',  ( -1.000000000000000000, -0.000000000000000000, -0.000000000000000000 ) ) ;
#3632=CIRCLE ( 'NONE', #426, 1.535500000000000087 ) ;
#3659=ORIENTED_EDGE ( 'NONE', *, *, #7703, .F. ) ;
#3665=DIRECTION ( 'NONE',  ( -1.000000000000000000, -0.000000000000000000, -0.000000000000000000 ) ) ;
#3666=AXIS2_PLACEMENT_3D ( 'NONE', #7990, #4768, #1203 ) ;
#3687=ORIENTED_EDGE ( 'NONE', *, *, #3883, .T. ) ;
#3695=DIRECTION ( 'NONE',  ( -1.000000000000000000, -0.000000000000000000, -0.000000000000000000 ) ) ;
#3708=ADVANCED_FACE ( 'NONE', ( #1191 ), #3032, .T. ) ;
#3719=EDGE_LOOP ( 'NONE', ( #10446, #5642, #7450, #6398, #1407 ) ) ;
#3725=VERTEX_POINT ( 'NONE', #352 ) ;
#3736=LINE ( 'NONE', #2912, #4232 ) ;
#3801=LINE ( 'NONE', #299, #7775 ) ;
#3823=DIRECTION ( 'NONE',  ( 0.000000000000000000, 0.000000000000000000, 1.000000000000000000 ) ) ;
#3827=AXIS2_PLACEMENT_3D ( 'NONE', #10010, #5787, #9172 ) ;
#3863=VERTEX_POINT ( 'NONE', #4857 ) ;
#3874=CIRCLE ( 'NONE', #9734, 0.2000000000000000944 ) ;
#3883=EDGE_CURVE ( 'NONE', #1907, #927, #5906, .T. ) ;
#3931=VECTOR ( 'NONE', #5738, 1000.000000000000227 ) ;
#3943=( LENGTH_UNIT ( ) NAMED_UNIT ( * ) SI_UNIT ( .MILLI., .METRE. ) );
#3962=EDGE_CURVE ( 'NONE', #1907, #7434, #2960, .T. ) ;
#3971=CARTESIAN_POINT ( 'NONE',  ( 0.000000000000000000, 0.8865213383406680414, -1.535500000000000975 ) ) ;
#3972=CARTESIAN_POINT ( 'NONE',  ( 2.000000000000000000, -1.502314598737159426E-15, -1.535500000000000087 ) ) ;
#3988=VERTEX_POINT ( 'NONE', #10697 ) ;
#4005=VERTEX_POINT ( 'NONE', #6373 ) ;
#4068=EDGE_LOOP ( 'NONE', ( #4858, #9181, #28, #7897 ) ) ;
#4079=VERTEX_POINT ( 'NONE', #5032 ) ;
#4115=DIRECTION ( 'NONE',  ( 0.000000000000000000, 0.4999999999999991118, -0.8660254037844390407 ) ) ;
#4138=DIRECTION ( 'NONE',  ( 1.000000000000000000, 0.000000000000000000, 0.000000000000000000 ) ) ;
#4153=CARTESIAN_POINT ( 'NONE',  ( 2.000000000000000000, 0.000000000000000000, 0.000000000000000000 ) ) ;
#4228=CARTESIAN_POINT ( 'NONE',  ( 2.886521338340684917, 0.000000000000000000, 0.000000000000000000 ) ) ;
#4232=VECTOR ( 'NONE', #10572, 1000.000000000000000 ) ;
#4250=CARTESIAN_POINT ( 'NONE',  ( 0.000000000000000000, 0.000000000000000000, 0.000000000000000000 ) ) ;
#4251=EDGE_LOOP ( 'NONE', ( #705, #2208, #4276 ) ) ;
#4272=VERTEX_POINT ( 'NONE', #9465 ) ;
#4276=ORIENTED_EDGE ( 'NONE', *, *, #7098, .F. ) ;
#4294=ORIENTED_EDGE ( 'NONE', *, *, #1393, .T. ) ;
#4296=DIRECTION ( 'NONE',  ( 0.000000000000000000, 0.000000000000000000, 1.000000000000000000 ) ) ;
#4324=EDGE_CURVE ( 'NONE', #7995, #5562, #6236, .T. ) ;
#4331=ADVANCED_FACE ( 'NONE', ( #185 ), #3584, .F. ) ;
#4338=DIRECTION ( 'NONE',  ( -1.000000000000000000, -0.000000000000000000, -0.000000000000000000 ) ) ;
#4350=VECTOR ( 'NONE', #5539, 1000.000000000000000 ) ;
#4351=EDGE_LOOP ( 'NONE', ( #3570, #4499 ) ) ;
#4353=CIRCLE ( 'NONE', #10555, 2.200000000000001066 ) ;
#4358=CLOSED_SHELL ( 'NONE', ( #1590, #4426, #5569, #6023, #7304, #146, #5928, #10211, #9636, #3708, #919, #10734, #6820, #1880, #6359, #10822, #291, #7027, #10353, #8376, #4331, #2333, #227, #1807, #440, #8998, #282 ) ) ;
#4396=ORIENTED_EDGE ( 'NONE', *, *, #10570, .F. ) ;
#4399=VECTOR ( 'NONE', #182, 1000.000000000000000 ) ;
#4413=VECTOR ( 'NONE', #9103, 1000.000000000000000 ) ;
#4421=AXIS2_PLACEMENT_3D ( 'NONE', #737, #4138, #7590 ) ;
#4426=ADVANCED_FACE ( 'NONE', ( #8875 ), #6857, .T. ) ;
#4449=EDGE_LOOP ( 'NONE', ( #9379, #8189, #3687, #2119 ) ) ;
#4453=SHAPE_DEFINITION_REPRESENTATION ( #9629, #1223 ) ;
#4462=DIRECTION ( 'NONE',  ( 0.000000000000000000, -0.5000000000000011102, -0.8660254037844379305 ) ) ;
#4476=DIRECTION ( 'NONE',  ( 0.000000000000000000, 0.000000000000000000, 1.000000000000000000 ) ) ;
#4482=SURFACE_SIDE_STYLE ('',( #1072 ) ) ;
#4491=DIRECTION ( 'NONE',  ( 1.000000000000000000, 0.000000000000000000, 0.000000000000000000 ) ) ;
#4499=ORIENTED_EDGE ( 'NONE', *, *, #7917, .T. ) ;
#4504=PLANE ( 'NONE',  #5247 ) ;
#4511=ORIENTED_EDGE ( 'NONE', *, *, #9537, .F. ) ;
#4545=CIRCLE ( 'NONE', #5774, 1.535500000000000087 ) ;
#4560=DIRECTION ( 'NONE',  ( 0.000000000000000000, -0.4999999999999991118, 0.8660254037844391517 ) ) ;
#4578=CIRCLE ( 'NONE', #9893, 0.2000000000000000944 ) ;
#4601=VECTOR ( 'NONE', #744, 1000.000000000000114 ) ;
#4609=CARTESIAN_POINT ( 'NONE',  ( 2.000000000000000000, 0.8865213383406680414, -1.535500000000000975 ) ) ;
#4636=ORIENTED_EDGE ( 'NONE', *, *, #743, .F. ) ;
#4641=CARTESIAN_POINT ( 'NONE',  ( 0.000000000000000000, 0.8865213383406680414, -1.535500000000000975 ) ) ;
#4687=DIRECTION ( 'NONE',  ( 0.000000000000000000, 0.000000000000000000, -1.000000000000000000 ) ) ;
#4701=AXIS2_PLACEMENT_3D ( 'NONE', #1604, #10271, #5990 ) ;
#4705=AXIS2_PLACEMENT_3D ( 'NONE', #2919, #1975, #9630 ) ;
#4723=ORIENTED_EDGE ( 'NONE', *, *, #4324, .F. ) ;
#4748=DIRECTION ( 'NONE',  ( 0.000000000000000000, 1.000000000000000000, -1.345283343056720273E-15 ) ) ;
#4749=EDGE_LOOP ( 'NONE', ( #1505, #6420, #5452, #699 ) ) ;
#4760=ORIENTED_EDGE ( 'NONE', *, *, #9317, .T. ) ;
#4768=DIRECTION ( 'NONE',  ( -1.000000000000000000, -0.000000000000000000, -0.000000000000000000 ) ) ;
#4770=LINE ( 'NONE', #6627, #3419 ) ;
#4791=SHAPE_REPRESENTATION_RELATIONSHIP ( 'NONE' , 'NONE' ,  #1223, #6261 ) ;
#4793=CARTESIAN_POINT ( 'NONE',  ( 4.000000000000001776, 0.000000000000000000, -2.200000000000001066 ) ) ;
#4821=DIRECTION ( 'NONE',  ( 0.000000000000000000, -0.5000000000000011102, -0.8660254037844379305 ) ) ;
#4823=EDGE_LOOP ( 'NONE', ( #8127, #3242 ) ) ;
#4825=CYLINDRICAL_SURFACE ( 'NONE', #7889, 2.000000000000000888 ) ;
#4838=ORIENTED_EDGE ( 'NONE', *, *, #10968, .T. ) ;
#4854=DIRECTION ( 'NONE',  ( 1.000000000000000000, 0.000000000000000000, 0.000000000000000000 ) ) ;
#4857=CARTESIAN_POINT ( 'NONE',  ( 2.000000000000000000, 1.329782007511006281, 0.7677499999999984892 ) ) ;
#4858=ORIENTED_EDGE ( 'NONE', *, *, #3519, .F. ) ;
#4871=DIRECTION ( 'NONE',  ( 0.000000000000000000, 0.000000000000000000, 1.000000000000000000 ) ) ;
#4883=VECTOR ( 'NONE', #9270, 1000.000000000000114 ) ;
#4884=VERTEX_POINT ( 'NONE', #10306 ) ;
#4885=DIRECTION ( 'NONE',  ( 0.000000000000000000, -1.224646799147353207E-16, 1.000000000000000000 ) ) ;
#4895=ORIENTED_EDGE ( 'NONE', *, *, #1713, .F. ) ;
#4906=FACE_OUTER_BOUND ( 'NONE', #155, .T. ) ;
#4926=LINE ( 'NONE', #8091, #2036 ) ;
#4937=VECTOR ( 'NONE', #4338, 1000.000000000000000 ) ;
#4958=( NAMED_UNIT ( * ) PLANE_ANGLE_UNIT ( ) SI_UNIT ( $, .RADIAN. ) );
#4959=CARTESIAN_POINT ( 'NONE',  ( -31.74999999999995737, 2.449293598294707893E-16, -2.000000000000000888 ) ) ;
#4965=ORIENTED_EDGE ( 'NONE', *, *, #3552, .T. ) ;
#4969=PLANE ( 'NONE',  #10034 ) ;
#4971=LINE ( 'NONE', #9023, #3931 ) ;
#4984=CARTESIAN_POINT ( 'NONE',  ( 2.000000000000000000, 1.773042676681340524, -2.059984127722458425E-15 ) ) ;
#5032=CARTESIAN_POINT ( 'NONE',  ( 0.1999999999999987899, 4.286263797015736595E-16, -3.500000000000000000 ) ) ;
#5043=EDGE_CURVE ( 'NONE', #233, #7995, #3315, .T. ) ;
#5055=DIRECTION ( 'NONE',  ( 0.000000000000000000, 0.000000000000000000, 1.000000000000000000 ) ) ;
#5056=EDGE_LOOP ( 'NONE', ( #3215, #7056 ) ) ;
#5058=LINE ( 'NONE', #930, #7347 ) ;
#5076=AXIS2_PLACEMENT_3D ( 'NONE', #7381, #7433, #1440 ) ;
#5081=CARTESIAN_POINT ( 'NONE',  ( 2.000000000000000000, 1.773042676681340524, -2.059984127722458425E-15 ) ) ;
#5112=EDGE_LOOP ( 'NONE', ( #6618, #3593, #376 ) ) ;
#5118=VECTOR ( 'NONE', #4748, 1000.000000000000000 ) ;
#5120=MECHANICAL_DESIGN_GEOMETRIC_PRESENTATION_REPRESENTATION('',(#9013),#1756);
#5132=CONICAL_SURFACE ( 'NONE', #496, 1.535500000000000087, 1.047197551196590748 ) ;
#5166=ORIENTED_EDGE ( 'NONE', *, *, #10355, .F. ) ;
#5174=DIRECTION ( 'NONE',  ( 0.000000000000000000, 0.000000000000000000, 1.000000000000000000 ) ) ;
#5207=CARTESIAN_POINT ( 'NONE',  ( 0.000000000000000000, 0.000000000000000000, 0.000000000000000000 ) ) ;
#5219=CARTESIAN_POINT ( 'NONE',  ( 0.000000000000000000, 4.163799117101000559E-16, -3.299999999999999822 ) ) ;
#5223=DIRECTION ( 'NONE',  ( 0.000000000000000000, -1.000000000000000000, 0.000000000000000000 ) ) ;
#5247=AXIS2_PLACEMENT_3D ( 'NONE', #6159, #266, #8717 ) ;
#5251=ORIENTED_EDGE ( 'NONE', *, *, #9317, .F. ) ;
#5278=DIRECTION ( 'NONE',  ( -1.000000000000000000, -0.000000000000000000, -0.000000000000000000 ) ) ;
#5287=CARTESIAN_POINT ( 'NONE',  ( 0.000000000000000000, 0.000000000000000000, 0.000000000000000000 ) ) ;
#5293=CIRCLE ( 'NONE', #7584, 2.200000000000001066 ) ;
#5311=FILL_AREA_STYLE_COLOUR ( '', #6459 ) ;
#5328=ORIENTED_EDGE ( 'NONE', *, *, #2925, .T. ) ;
#5333=EDGE_CURVE ( 'NONE', #9782, #4079, #3736, .T. ) ;
#5367=DIRECTION ( 'NONE',  ( -1.000000000000000000, -0.000000000000000000, -0.000000000000000000 ) ) ;
#5369=CARTESIAN_POINT ( 'NONE',  ( 2.000000000000000000, -0.8865213383406730374, -1.535499999999999421 ) ) ;
#5372=AXIS2_PLACEMENT_3D ( 'NONE', #10543, #10437, #9764 ) ;
#5412=CARTESIAN_POINT ( 'NONE',  ( 2.000000000000000000, -0.8865213383406694847, 1.535500000000001419 ) ) ;
#5426=VECTOR ( 'NONE', #6414, 1000.000000000000000 ) ;
#5432=CARTESIAN_POINT ( 'NONE',  ( 4.000000000000003553, 0.000000000000000000, 0.000000000000000000 ) ) ;
#5436=LINE ( 'NONE', #8760, #7856 ) ;
#5444=LINE ( 'NONE', #10503, #10028 ) ;
#5445=AXIS2_PLACEMENT_3D ( 'NONE', #1138, #1199, #9702 ) ;
#5452=ORIENTED_EDGE ( 'NONE', *, *, #8466, .T. ) ;
#5458=DIRECTION ( 'NONE',  ( 1.000000000000000000, 0.000000000000000000, 0.000000000000000000 ) ) ;
#5464=DIRECTION ( 'NONE',  ( 0.000000000000000000, 0.000000000000000000, 1.000000000000000000 ) ) ;
#5469=EDGE_CURVE ( 'NONE', #4079, #3081, #3874, .T. ) ;
#5492=PLANE ( 'NONE',  #7726 ) ;
#5508=ORIENTED_EDGE ( 'NONE', *, *, #10570, .T. ) ;
#5534=EDGE_LOOP ( 'NONE', ( #10246, #4895, #2313, #8374 ) ) ;
#5539=DIRECTION ( 'NONE',  ( -0.7071067811865292541, 8.659560562355155958E-17, -0.7071067811865657804 ) ) ;
#5555=VECTOR ( 'NONE', #4462, 1000.000000000000114 ) ;
#5562=VERTEX_POINT ( 'NONE', #2660 ) ;
#5569=ADVANCED_FACE ( 'NONE', ( #194 ), #7248, .F. ) ;
#5579=CIRCLE ( 'NONE', #762, 1.610000000000000098 ) ;
#5586=VERTEX_POINT ( 'NONE', #5369 ) ;
#5627=DIRECTION ( 'NONE',  ( 0.000000000000000000, 0.000000000000000000, -1.000000000000000000 ) ) ;
#5629=ORIENTED_EDGE ( 'NONE', *, *, #3962, .T. ) ;
#5642=ORIENTED_EDGE ( 'NONE', *, *, #10214, .F. ) ;
#5692=ORIENTED_EDGE ( 'NONE', *, *, #10625, .T. ) ;
#5723=SURFACE_SIDE_STYLE ('',( #2330 ) ) ;
#5736=CYLINDRICAL_SURFACE ( 'NONE', #2399, 3.500000000000000000 ) ;
#5737=FACE_OUTER_BOUND ( 'NONE', #7717, .T. ) ;
#5738=DIRECTION ( 'NONE',  ( 0.000000000000000000, 0.4999999999999989453, -0.8660254037844391517 ) ) ;
#5774=AXIS2_PLACEMENT_3D ( 'NONE', #1266, #9816, #7993 ) ;
#5787=DIRECTION ( 'NONE',  ( -1.000000000000000000, -0.000000000000000000, -0.000000000000000000 ) ) ;
#5834=SURFACE_STYLE_USAGE ( .BOTH. , #5723 ) ;
#5889=DIRECTION ( 'NONE',  ( 0.000000000000000000, 0.000000000000000000, 1.000000000000000000 ) ) ;
#5906=LINE ( 'NONE', #3130, #8260 ) ;
#5908=PLANE ( 'NONE',  #2632 ) ;
#5920=ORIENTED_EDGE ( 'NONE', *, *, #4324, .T. ) ;
#5928=ADVANCED_FACE ( 'NONE', ( #2583, #10966 ), #5908, .T. ) ;
#5941=LINE ( 'NONE', #7837, #6292 ) ;
#5964=CARTESIAN_POINT ( 'NONE',  ( 2.000000000000000000, 0.8865213383406680414, -1.535500000000000975 ) ) ;
#5978=ORIENTED_EDGE ( 'NONE', *, *, #3883, .F. ) ;
#5989=EDGE_LOOP ( 'NONE', ( #4760, #2797, #2170, #9518, #6880 ) ) ;
#5990=DIRECTION ( 'NONE',  ( 0.000000000000000000, -0.4999999999999989453, 0.8660254037844391517 ) ) ;
#5991=DIRECTION ( 'NONE',  ( -0.5000000000000061062, 0.000000000000000000, 0.8660254037844351549 ) ) ;
#5992=PRODUCT_CONTEXT ( 'NONE', #10820, 'mechanical' ) ;
#6003=EDGE_CURVE ( 'NONE', #7695, #10667, #4578, .T. ) ;
#6023=ADVANCED_FACE ( 'NONE', ( #11 ), #134, .T. ) ;
#6024=ORIENTED_EDGE ( 'NONE', *, *, #7878, .T. ) ;
#6049=EDGE_CURVE ( 'NONE', #3226, #5586, #10187, .T. ) ;
#6068=AXIS2_PLACEMENT_3D ( 'NONE', #940, #1899, #1103 ) ;
#6070=CARTESIAN_POINT ( 'NONE',  ( 11.99999999999999645, 0.000000000000000000, 0.000000000000000000 ) ) ;
#6082=DIRECTION ( 'NONE',  ( 0.000000000000000000, 0.4999999999999989453, -0.8660254037844391517 ) ) ;
#6094=ORIENTED_EDGE ( 'NONE', *, *, #3519, .T. ) ;
#6103=CIRCLE ( 'NONE', #8600, 1.610000000000000098 ) ;
#6112=ORIENTED_EDGE ( 'NONE', *, *, #10758, .F. ) ;
#6136=DIRECTION ( 'NONE',  ( 1.000000000000000000, 0.000000000000000000, 0.000000000000000000 ) ) ;
#6156=DIRECTION ( 'NONE',  ( 0.000000000000000000, 0.000000000000000000, 1.000000000000000000 ) ) ;
#6159=CARTESIAN_POINT ( 'NONE',  ( 2.000000000000000000, 1.773042676681340524, -2.059984127722458425E-15 ) ) ;
#6172=CIRCLE ( 'NONE', #7948, 1.535500000000000087 ) ;
#6190=FACE_OUTER_BOUND ( 'NONE', #4749, .T. ) ;
#6221=ORIENTED_EDGE ( 'NONE', *, *, #2254, .T. ) ;
#6236=LINE ( 'NONE', #5412, #3487 ) ;
#6261=ADVANCED_BREP_SHAPE_REPRESENTATION ( '', ( #9072, #308 ), #7601 ) ;
#6270=ORIENTED_EDGE ( 'NONE', *, *, #8301, .T. ) ;
#6283=FACE_OUTER_BOUND ( 'NONE', #449, .T. ) ;
#6292=VECTOR ( 'NONE', #210, 1000.000000000000000 ) ;
#6298=DIRECTION ( 'NONE',  ( 0.000000000000000000, 0.000000000000000000, -1.000000000000000000 ) ) ;
#6301=EDGE_CURVE ( 'NONE', #233, #1715, #7447, .T. ) ;
#6323=LINE ( 'NONE', #8833, #8613 ) ;
#6343=AXIS2_PLACEMENT_3D ( 'NONE', #6070, #8633, #4476 ) ;
#6344=AXIS2_PLACEMENT_3D ( 'NONE', #2448, #9387, #7617 ) ;
#6359=ADVANCED_FACE ( 'NONE', ( #4906 ), #7282, .T. ) ;
#6373=CARTESIAN_POINT ( 'NONE',  ( 0.000000000000000000, 1.773042676681340524, -2.059984127722458425E-15 ) ) ;
#6398=ORIENTED_EDGE ( 'NONE', *, *, #635, .F. ) ;
#6414=DIRECTION ( 'NONE',  ( 0.000000000000000000, 1.000000000000000000, -1.345283343056720273E-15 ) ) ;
#6420=ORIENTED_EDGE ( 'NONE', *, *, #9626, .T. ) ;
#6424=VERTEX_POINT ( 'NONE', #2682 ) ;
#6426=CARTESIAN_POINT ( 'NONE',  ( 4.200000000000001954, 0.000000000000000000, 0.000000000000000000 ) ) ;
#6442=PLANE ( 'NONE',  #10730 ) ;
#6453=DIRECTION ( 'NONE',  ( 0.000000000000000000, 0.000000000000000000, 1.000000000000000000 ) ) ;
#6459=COLOUR_RGB ( '', 0.31764706, 0.68627451, 0.89019608) ;
#6493=( NAMED_UNIT ( * ) PLANE_ANGLE_UNIT ( ) SI_UNIT ( $, .RADIAN. ) );
#6500=PRODUCT_DEFINITION_FORMATION_WITH_SPECIFIED_SOURCE ( 'ANY', '', #7680, .NOT_KNOWN. ) ;
#6510=ORIENTED_EDGE ( 'NONE', *, *, #10590, .F. ) ;
#6521=FACE_OUTER_BOUND ( 'NONE', #6954, .T. ) ;
#6528=PRODUCT_DEFINITION ( 'UNKNOWN', '', #6500, #10891 ) ;
#6609=LINE ( 'NONE', #8397, #9600 ) ;
#6616=ORIENTED_EDGE ( 'NONE', *, *, #7769, .F. ) ;
#6618=ORIENTED_EDGE ( 'NONE', *, *, #8406, .F. ) ;
#6627=CARTESIAN_POINT ( 'NONE',  ( 2.000000000000000000, -0.8865213383406694847, 1.535500000000001419 ) ) ;
#6638=( GEOMETRIC_REPRESENTATION_CONTEXT ( 3 ) GLOBAL_UNCERTAINTY_ASSIGNED_CONTEXT ( ( #7586 ) ) GLOBAL_UNIT_ASSIGNED_CONTEXT ( ( #8442, #4958, #6657 ) ) REPRESENTATION_CONTEXT ( 'NONE', 'WORKASPACE' ) );
#6639=AXIS2_PLACEMENT_3D ( 'NONE', #1685, #3471, #10299 ) ;
#6654=FILL_AREA_STYLE ('',( #10881 ) ) ;
#6655=VECTOR ( 'NONE', #4821, 1000.000000000000114 ) ;
#6657=( NAMED_UNIT ( * ) SI_UNIT ( $, .STERADIAN. ) SOLID_ANGLE_UNIT ( ) );
#6732=LINE ( 'NONE', #2575, #444 ) ;
#6765=DIRECTION ( 'NONE',  ( -0.7071067811865292541, 0.000000000000000000, 0.7071067811865657804 ) ) ;
#6794=ORIENTED_EDGE ( 'NONE', *, *, #1624, .T. ) ;
#6820=ADVANCED_FACE ( 'NONE', ( #10666 ), #8967, .F. ) ;
#6857=TOROIDAL_SURFACE ( 'NONE', #5445, 3.299999999999999822, 0.2000000000000000111 ) ;
#6880=ORIENTED_EDGE ( 'NONE', *, *, #1517, .T. ) ;
#6897=CARTESIAN_POINT ( 'NONE',  ( 0.000000000000000000, 0.000000000000000000, 3.299999999999999822 ) ) ;
#6912=DIRECTION ( 'NONE',  ( -1.000000000000000000, -0.000000000000000000, -0.000000000000000000 ) ) ;
#6954=EDGE_LOOP ( 'NONE', ( #3659, #3604, #10314, #4965, #1045 ) ) ;
#6956=CARTESIAN_POINT ( 'NONE',  ( 0.000000000000000000, 0.000000000000000000, 0.000000000000000000 ) ) ;
#6996=LINE ( 'NONE', #10331, #4883 ) ;
#7017=AXIS2_PLACEMENT_3D ( 'NONE', #2861, #9682, #9515 ) ;
#7022=PLANE ( 'NONE',  #7017 ) ;
#7027=ADVANCED_FACE ( 'NONE', ( #9209 ), #9263, .T. ) ;
#7056=ORIENTED_EDGE ( 'NONE', *, *, #7861, .F. ) ;
#7098=EDGE_CURVE ( 'NONE', #7995, #1715, #9656, .T. ) ;
#7146=DIRECTION ( 'NONE',  ( -1.000000000000000000, -0.000000000000000000, -0.000000000000000000 ) ) ;
#7201=FACE_BOUND ( 'NONE', #4351, .T. ) ;
#7208=DIRECTION ( 'NONE',  ( -1.000000000000000000, -0.000000000000000000, -0.000000000000000000 ) ) ;
#7220=ORIENTED_EDGE ( 'NONE', *, *, #5469, .T. ) ;
#7239=CARTESIAN_POINT ( 'NONE',  ( -31.74999999999995737, 0.000000000000000000, 0.000000000000000000 ) ) ;
#7240=CIRCLE ( 'NONE', #9554, 3.299999999999999822 ) ;
#7248=TOROIDAL_SURFACE ( 'NONE', #8676, 2.200000000000001066, 0.2000000000000000111 ) ;
#7258=CARTESIAN_POINT ( 'NONE',  ( 4.000000000000001776, 2.694222958124178486E-16, 2.200000000000001066 ) ) ;
#7282=PLANE ( 'NONE',  #7955 ) ;
#7304=ADVANCED_FACE ( 'NONE', ( #3048 ), #4825, .T. ) ;
#7347=VECTOR ( 'NONE', #6765, 1000.000000000000000 ) ;
#7351=ORIENTED_EDGE ( 'NONE', *, *, #5043, .T. ) ;
#7369=AXIS2_PLACEMENT_3D ( 'NONE', #8870, #8811, #6453 ) ;
#7381=CARTESIAN_POINT ( 'NONE',  ( 4.200000000000001954, 0.000000000000000000, 0.000000000000000000 ) ) ;
#7385=VERTEX_POINT ( 'NONE', #641 ) ;
#7423=EDGE_CURVE ( 'NONE', #6424, #10663, #5579, .T. ) ;
#7430=DIRECTION ( 'NONE',  ( -0.000000000000000000, 1.000000000000000000, 1.224646799147353207E-16 ) ) ;
#7433=DIRECTION ( 'NONE',  ( 1.000000000000000000, 0.000000000000000000, 0.000000000000000000 ) ) ;
#7434=VERTEX_POINT ( 'NONE', #2537 ) ;
#7446=FACE_OUTER_BOUND ( 'NONE', #5112, .T. ) ;
#7447=LINE ( 'NONE', #10890, #5118 ) ;
#7450=ORIENTED_EDGE ( 'NONE', *, *, #8301, .F. ) ;
#7456=PLANE ( 'NONE',  #7465 ) ;
#7462=VERTEX_POINT ( 'NONE', #9369 ) ;
#7465=AXIS2_PLACEMENT_3D ( 'NONE', #5081, #4854, #10899 ) ;
#7495=CIRCLE ( 'NONE', #9450, 3.299999999999999822 ) ;
#7497=DIRECTION ( 'NONE',  ( 0.000000000000000000, -1.000000000000000000, 1.345283343056720273E-15 ) ) ;
#7510=DIRECTION ( 'NONE',  ( 0.000000000000000000, -9.783878858594328898E-16, -1.000000000000000000 ) ) ;
#7531=ORIENTED_EDGE ( 'NONE', *, *, #1533, .T. ) ;
#7547=DIRECTION ( 'NONE',  ( -1.000000000000000000, -0.000000000000000000, -0.000000000000000000 ) ) ;
#7554=( LENGTH_UNIT ( ) NAMED_UNIT ( * ) SI_UNIT ( .MILLI., .METRE. ) );
#7555=AXIS2_PLACEMENT_3D ( 'NONE', #10313, #5367, #8750 ) ;
#7576=CARTESIAN_POINT ( 'NONE',  ( 2.000000000000000000, 1.773042676681340524, -2.059984127722458425E-15 ) ) ;
#7584=AXIS2_PLACEMENT_3D ( 'NONE', #386, #2742, #10346 ) ;
#7586=UNCERTAINTY_MEASURE_WITH_UNIT (LENGTH_MEASURE( 1.000000000000000082E-05 ), #8442, 'distance_accuracy_value', 'NONE');
#7590=DIRECTION ( 'NONE',  ( 0.000000000000000000, 0.000000000000000000, 1.000000000000000000 ) ) ;
#7601=( GEOMETRIC_REPRESENTATION_CONTEXT ( 3 ) GLOBAL_UNCERTAINTY_ASSIGNED_CONTEXT ( ( #1084 ) ) GLOBAL_UNIT_ASSIGNED_CONTEXT ( ( #3943, #6493, #1609 ) ) REPRESENTATION_CONTEXT ( 'NONE', 'WORKASPACE' ) );
#7617=DIRECTION ( 'NONE',  ( 0.000000000000000000, 0.000000000000000000, -1.000000000000000000 ) ) ;
#7680=PRODUCT ( 'socket head cap screw_iso_ISO 4762 M4 x 8 - 8N', 'socket head cap screw_iso_ISO 4762 M4 x 8 - 8N', '', ( #5992 ) ) ;
#7694=ORIENTED_EDGE ( 'NONE', *, *, #8466, .F. ) ;
#7695=VERTEX_POINT ( 'NONE', #989 ) ;
#7703=EDGE_CURVE ( 'NONE', #10716, #1715, #10273, .T. ) ;
#7717=EDGE_LOOP ( 'NONE', ( #2545, #4723, #9545 ) ) ;
#7726=AXIS2_PLACEMENT_3D ( 'NONE', #8820, #2993, #10540 ) ;
#7750=DIRECTION ( 'NONE',  ( -1.000000000000000000, 0.000000000000000000, -0.000000000000000000 ) ) ;
#7769=EDGE_CURVE ( 'NONE', #6424, #1907, #5058, .T. ) ;
#7775=VECTOR ( 'NONE', #3695, 1000.000000000000000 ) ;
#7777=ORIENTED_EDGE ( 'NONE', *, *, #743, .T. ) ;
#7814=FACE_OUTER_BOUND ( 'NONE', #2610, .T. ) ;
#7828=ORIENTED_EDGE ( 'NONE', *, *, #2254, .F. ) ;
#7837=CARTESIAN_POINT ( 'NONE',  ( 0.000000000000000000, -0.8865213383406694847, 1.535500000000001419 ) ) ;
#7841=EDGE_CURVE ( 'NONE', #3725, #932, #10197, .T. ) ;
#7856=VECTOR ( 'NONE', #2042, 1000.000000000000000 ) ;
#7861=EDGE_CURVE ( 'NONE', #10663, #6424, #6103, .T. ) ;
#7870=CARTESIAN_POINT ( 'NONE',  ( 2.000000000000000000, 1.773042676681340524, -2.059984127722458425E-15 ) ) ;
#7878=EDGE_CURVE ( 'NONE', #1715, #3863, #3632, .T. ) ;
#7886=CARTESIAN_POINT ( 'NONE',  ( 4.000000000000000000, 0.000000000000000000, 0.000000000000000000 ) ) ;
#7889=AXIS2_PLACEMENT_3D ( 'NONE', #10657, #7208, #8255 ) ;
#7891=CARTESIAN_POINT ( 'NONE',  ( 0.000000000000000000, -0.8865213383406730374, -1.535499999999999421 ) ) ;
#7893=VECTOR ( 'NONE', #5991, 1000.000000000000000 ) ;
#7897=ORIENTED_EDGE ( 'NONE', *, *, #7917, .F. ) ;
#7903=VECTOR ( 'NONE', #6912, 1000.000000000000000 ) ;
#7917=EDGE_CURVE ( 'NONE', #1487, #10667, #4353, .T. ) ;
#7948=AXIS2_PLACEMENT_3D ( 'NONE', #8384, #9218, #5174 ) ;
#7955=AXIS2_PLACEMENT_3D ( 'NONE', #1405, #10677, #4115 ) ;
#7990=CARTESIAN_POINT ( 'NONE',  ( 11.61000000000001542, 0.000000000000000000, 0.000000000000000000 ) ) ;
#7993=DIRECTION ( 'NONE',  ( 0.000000000000000000, 0.000000000000000000, 1.000000000000000000 ) ) ;
#7995=VERTEX_POINT ( 'NONE', #1095 ) ;
#8020=EDGE_LOOP ( 'NONE', ( #10188, #3347, #6024, #2442, #2063 ) ) ;
#8026=CIRCLE ( 'NONE', #2345, 1.535500000000000087 ) ;
#8064=DIRECTION ( 'NONE',  ( -1.000000000000000000, -0.000000000000000000, -0.000000000000000000 ) ) ;
#8091=CARTESIAN_POINT ( 'NONE',  ( 2.000000000000000000, -0.8865213383406730374, -1.535499999999999421 ) ) ;
#8096=AXIS2_PLACEMENT_3D ( 'NONE', #10470, #2864, #8636 ) ;
#8099=DIRECTION ( 'NONE',  ( -1.000000000000000000, -0.000000000000000000, -0.000000000000000000 ) ) ;
#8127=ORIENTED_EDGE ( 'NONE', *, *, #1393, .F. ) ;
#8149=DIRECTION ( 'NONE',  ( -1.000000000000000000, -0.000000000000000000, -0.000000000000000000 ) ) ;
#8189=ORIENTED_EDGE ( 'NONE', *, *, #10345, .T. ) ;
#8214=ORIENTED_EDGE ( 'NONE', *, *, #10789, .T. ) ;
#8226=DIRECTION ( 'NONE',  ( -1.000000000000000000, -0.000000000000000000, -0.000000000000000000 ) ) ;
#8233=AXIS2_PLACEMENT_3D ( 'NONE', #1829, #5223, #10109 ) ;
#8241=AXIS2_PLACEMENT_3D ( 'NONE', #6426, #423, #10551 ) ;
#8255=DIRECTION ( 'NONE',  ( 0.000000000000000000, 0.000000000000000000, 1.000000000000000000 ) ) ;
#8260=VECTOR ( 'NONE', #1574, 1000.000000000000000 ) ;
#8301=EDGE_CURVE ( 'NONE', #7385, #1406, #6996, .T. ) ;
#8304=EDGE_CURVE ( 'NONE', #927, #7695, #3104, .T. ) ;
#8305=DIRECTION ( 'NONE',  ( 0.000000000000000000, -1.000000000000000000, 9.783878858594328898E-16 ) ) ;
#8374=ORIENTED_EDGE ( 'NONE', *, *, #1624, .F. ) ;
#8376=ADVANCED_FACE ( 'NONE', ( #10660 ), #4504, .F. ) ;
#8384=CARTESIAN_POINT ( 'NONE',  ( 2.000000000000000000, 0.000000000000000000, 0.000000000000000000 ) ) ;
#8387=CARTESIAN_POINT ( 'NONE',  ( 0.1999999999999987899, 0.000000000000000000, 0.000000000000000000 ) ) ;
#8397=CARTESIAN_POINT ( 'NONE',  ( 2.000000000000000000, 1.773042676681340524, -2.059984127722458425E-15 ) ) ;
#8403=ORIENTED_EDGE ( 'NONE', *, *, #6049, .T. ) ;
#8406=EDGE_CURVE ( 'NONE', #1703, #3863, #5444, .T. ) ;
#8414=DIRECTION ( 'NONE',  ( -1.000000000000000000, -0.000000000000000000, -0.000000000000000000 ) ) ;
#8425=DIRECTION ( 'NONE',  ( 0.000000000000000000, 0.000000000000000000, 1.000000000000000000 ) ) ;
#8442=( LENGTH_UNIT ( ) NAMED_UNIT ( * ) SI_UNIT ( .MILLI., .METRE. ) );
#8465=CARTESIAN_POINT ( 'NONE',  ( 4.200000000000001954, 0.000000000000000000, -2.200000000000001066 ) ) ;
#8466=EDGE_CURVE ( 'NONE', #9720, #3725, #6323, .T. ) ;
#8535=LINE ( 'NONE', #1699, #3001 ) ;
#8543=DIRECTION ( 'NONE',  ( -1.000000000000000000, -0.000000000000000000, -0.000000000000000000 ) ) ;
#8585=DIRECTION ( 'NONE',  ( 0.000000000000000000, 0.000000000000000000, 1.000000000000000000 ) ) ;
#8600=AXIS2_PLACEMENT_3D ( 'NONE', #2782, #5278, #2890 ) ;
#8613=VECTOR ( 'NONE', #3665, 1000.000000000000000 ) ;
#8625=ORIENTED_EDGE ( 'NONE', *, *, #8653, .T. ) ;
#8633=DIRECTION ( 'NONE',  ( -1.000000000000000000, -0.000000000000000000, -0.000000000000000000 ) ) ;
#8636=DIRECTION ( 'NONE',  ( 0.000000000000000000, 0.000000000000000000, -1.000000000000000000 ) ) ;
#8653=EDGE_CURVE ( 'NONE', #10663, #7434, #1139, .T. ) ;
#8665=DIRECTION ( 'NONE',  ( -1.000000000000000000, -0.000000000000000000, -0.000000000000000000 ) ) ;
#8676=AXIS2_PLACEMENT_3D ( 'NONE', #2711, #4491, #248 ) ;
#8696=FILL_AREA_STYLE ('',( #5311 ) ) ;
#8699=DIRECTION ( 'NONE',  ( 0.000000000000000000, -0.5000000000000011102, -0.8660254037844379305 ) ) ;
#8711=ORIENTED_EDGE ( 'NONE', *, *, #8653, .F. ) ;
#8717=DIRECTION ( 'NONE',  ( 0.000000000000000000, 0.5000000000000011102, 0.8660254037844379305 ) ) ;
#8733=DIRECTION ( 'NONE',  ( 0.000000000000000000, 0.000000000000000000, 1.000000000000000000 ) ) ;
#8740=DIRECTION ( 'NONE',  ( 0.000000000000000000, -0.5000000000000011102, -0.8660254037844379305 ) ) ;
#8750=DIRECTION ( 'NONE',  ( 0.000000000000000000, 0.000000000000000000, 1.000000000000000000 ) ) ;
#8760=CARTESIAN_POINT ( 'NONE',  ( 2.000000000000000000, 1.880445160090761061E-16, -1.535500000000000087 ) ) ;
#8780=VECTOR ( 'NONE', #8543, 1000.000000000000000 ) ;
#8806=LINE ( 'NONE', #1249, #2263 ) ;
#8811=DIRECTION ( 'NONE',  ( -1.000000000000000000, -0.000000000000000000, -0.000000000000000000 ) ) ;
#8820=CARTESIAN_POINT ( 'NONE',  ( 4.000000000000000000, 3.500000000000000000, 0.000000000000000000 ) ) ;
#8829=EDGE_CURVE ( 'NONE', #5586, #9268, #4926, .T. ) ;
#8833=CARTESIAN_POINT ( 'NONE',  ( -31.74999999999995737, 0.000000000000000000, 3.500000000000000000 ) ) ;
#8837=ORIENTED_EDGE ( 'NONE', *, *, #7878, .F. ) ;
#8858=ORIENTED_EDGE ( 'NONE', *, *, #10214, .T. ) ;
#8870=CARTESIAN_POINT ( 'NONE',  ( -31.74999999999995737, 0.000000000000000000, 0.000000000000000000 ) ) ;
#8875=FACE_OUTER_BOUND ( 'NONE', #479, .T. ) ;
#8889=ORIENTED_EDGE ( 'NONE', *, *, #10906, .T. ) ;
#8967=TOROIDAL_SURFACE ( 'NONE', #5076, 2.200000000000001066, 0.2000000000000000111 ) ;
#8998=ADVANCED_FACE ( 'NONE', ( #7814 ), #296, .F. ) ;
#9009=CARTESIAN_POINT ( 'NONE',  ( 2.000000000000000000, 0.8865213383406680414, -1.535500000000000975 ) ) ;
#9013=STYLED_ITEM ( 'NONE', ( #9216 ), #6261 ) ;
#9023=CARTESIAN_POINT ( 'NONE',  ( 2.000000000000000000, -1.773042676681341856, 2.276824562219559311E-15 ) ) ;
#9032=CARTESIAN_POINT ( 'NONE',  ( 4.000000000000003553, 4.286263797015736595E-16, -3.500000000000000000 ) ) ;
#9072=MANIFOLD_SOLID_BREP ( 'Hex', #4358 ) ;
#9081=DIRECTION ( 'NONE',  ( -1.000000000000000000, -0.000000000000000000, -0.000000000000000000 ) ) ;
#9103=DIRECTION ( 'NONE',  ( 0.000000000000000000, -1.000000000000000000, 9.783878858594328898E-16 ) ) ;
#9126=CIRCLE ( 'NONE', #8241, 2.000000000000000888 ) ;
#9137=CIRCLE ( 'NONE', #3827, 2.000000000000000888 ) ;
#9172=DIRECTION ( 'NONE',  ( 0.000000000000000000, 0.000000000000000000, 1.000000000000000000 ) ) ;
#9181=ORIENTED_EDGE ( 'NONE', *, *, #9464, .F. ) ;
#9209=FACE_OUTER_BOUND ( 'NONE', #2735, .T. ) ;
#9216=PRESENTATION_STYLE_ASSIGNMENT (( #5834 ) ) ;
#9218=DIRECTION ( 'NONE',  ( -1.000000000000000000, -0.000000000000000000, -0.000000000000000000 ) ) ;
#9223=EDGE_LOOP ( 'NONE', ( #872, #7828, #8837 ) ) ;
#9263=PLANE ( 'NONE',  #4701 ) ;
#9268=VERTEX_POINT ( 'NONE', #7891 ) ;
#9270=DIRECTION ( 'NONE',  ( 0.000000000000000000, -0.5000000000000011102, -0.8660254037844379305 ) ) ;
#9290=CYLINDRICAL_SURFACE ( 'NONE', #6639, 3.500000000000000000 ) ;
#9317=EDGE_CURVE ( 'NONE', #4272, #3988, #5941, .T. ) ;
#9331=LINE ( 'NONE', #4959, #4937 ) ;
#9369=CARTESIAN_POINT ( 'NONE',  ( 0.000000000000000000, -1.773042676681341856, 2.276824562219559311E-15 ) ) ;
#9373=LINE ( 'NONE', #1771, #9492 ) ;
#9379=ORIENTED_EDGE ( 'NONE', *, *, #10789, .F. ) ;
#9387=DIRECTION ( 'NONE',  ( 1.000000000000000000, 0.000000000000000000, 0.000000000000000000 ) ) ;
#9450=AXIS2_PLACEMENT_3D ( 'NONE', #5287, #477, #1378 ) ;
#9464=EDGE_CURVE ( 'NONE', #7695, #927, #9126, .T. ) ;
#9465=CARTESIAN_POINT ( 'NONE',  ( 0.000000000000000000, -0.8865213383406694847, 1.535500000000001419 ) ) ;
#9478=EDGE_CURVE ( 'NONE', #7462, #9268, #9373, .T. ) ;
#9492=VECTOR ( 'NONE', #922, 1000.000000000000227 ) ;
#9515=DIRECTION ( 'NONE',  ( 0.000000000000000000, 0.5000000000000011102, 0.8660254037844379305 ) ) ;
#9516=DIRECTION ( 'NONE',  ( 0.000000000000000000, -1.000000000000000000, 0.000000000000000000 ) ) ;
#9518=ORIENTED_EDGE ( 'NONE', *, *, #6301, .F. ) ;
#9537=EDGE_CURVE ( 'NONE', #5562, #7462, #10321, .T. ) ;
#9545=ORIENTED_EDGE ( 'NONE', *, *, #3552, .F. ) ;
#9554=AXIS2_PLACEMENT_3D ( 'NONE', #5207, #8414, #8585 ) ;
#9558=LINE ( 'NONE', #3096, #5555 ) ;
#9565=DIRECTION ( 'NONE',  ( 1.000000000000000000, 0.000000000000000000, 0.000000000000000000 ) ) ;
#9571=CARTESIAN_POINT ( 'NONE',  ( 2.000000000000000000, -0.8865213383406694847, 1.535500000000001419 ) ) ;
#9600=VECTOR ( 'NONE', #10793, 1000.000000000000000 ) ;
#9626=EDGE_CURVE ( 'NONE', #9782, #9720, #83, .T. ) ;
#9629=PRODUCT_DEFINITION_SHAPE ( 'NONE', 'NONE',  #6528 ) ;
#9630=DIRECTION ( 'NONE',  ( 0.000000000000000000, 0.000000000000000000, -1.000000000000000000 ) ) ;
#9636=ADVANCED_FACE ( 'NONE', ( #7201, #359 ), #5492, .T. ) ;
#9656=CIRCLE ( 'NONE', #246, 1.535500000000000087 ) ;
#9662=ORIENTED_EDGE ( 'NONE', *, *, #7841, .F. ) ;
#9665=ORIENTED_EDGE ( 'NONE', *, *, #8829, .F. ) ;
#9667=ORIENTED_EDGE ( 'NONE', *, *, #1533, .F. ) ;
#9682=DIRECTION ( 'NONE',  ( 0.000000000000000000, 0.8660254037844380415, -0.5000000000000012212 ) ) ;
#9702=DIRECTION ( 'NONE',  ( 0.000000000000000000, 0.000000000000000000, 1.000000000000000000 ) ) ;
#9720=VERTEX_POINT ( 'NONE', #411 ) ;
#9729=AXIS2_PLACEMENT_3D ( 'NONE', #7870, #6136, #6298 ) ;
#9734=AXIS2_PLACEMENT_3D ( 'NONE', #10709, #7430, #4885 ) ;
#9755=EDGE_CURVE ( 'NONE', #1715, #10456, #10650, .T. ) ;
#9759=CARTESIAN_POINT ( 'NONE',  ( 11.99999999999999645, 1.971681346627238735E-16, -1.610000000000000098 ) ) ;
#9764=DIRECTION ( 'NONE',  ( 0.000000000000000000, 0.000000000000000000, 1.000000000000000000 ) ) ;
#9765=CARTESIAN_POINT ( 'NONE',  ( 0.000000000000000000, 1.773042676681340524, -2.059984127722458425E-15 ) ) ;
#9778=ORIENTED_EDGE ( 'NONE', *, *, #10355, .T. ) ;
#9782=VERTEX_POINT ( 'NONE', #9032 ) ;
#9797=VECTOR ( 'NONE', #8305, 1000.000000000000000 ) ;
#9816=DIRECTION ( 'NONE',  ( -1.000000000000000000, -0.000000000000000000, -0.000000000000000000 ) ) ;
#9846=ORIENTED_EDGE ( 'NONE', *, *, #6049, .F. ) ;
#9893=AXIS2_PLACEMENT_3D ( 'NONE', #8465, #9516, #10245 ) ;
#9896=LINE ( 'NONE', #9009, #4413 ) ;
#9924=CARTESIAN_POINT ( 'NONE',  ( 2.000000000000000000, 0.000000000000000000, 0.000000000000000000 ) ) ;
#10010=CARTESIAN_POINT ( 'NONE',  ( 11.61000000000001542, 0.000000000000000000, 0.000000000000000000 ) ) ;
#10028=VECTOR ( 'NONE', #4560, 1000.000000000000000 ) ;
#10034=AXIS2_PLACEMENT_3D ( 'NONE', #722, #7510, #10958 ) ;
#10082=EDGE_LOOP ( 'NONE', ( #4294, #621, #5508, #7694 ) ) ;
#10109=DIRECTION ( 'NONE',  ( 0.000000000000000000, 0.000000000000000000, -1.000000000000000000 ) ) ;
#10123=EDGE_LOOP ( 'NONE', ( #8403, #3268, #539 ) ) ;
#10181=DIRECTION ( 'NONE',  ( 0.000000000000000000, -0.4999999999999991118, 0.8660254037844391517 ) ) ;
#10187=LINE ( 'NONE', #5964, #4399 ) ;
#10188=ORIENTED_EDGE ( 'NONE', *, *, #1272, .F. ) ;
#10197=CIRCLE ( 'NONE', #8233, 0.2000000000000000944 ) ;
#10211=ADVANCED_FACE ( 'NONE', ( #6190 ), #5736, .T. ) ;
#10214=EDGE_CURVE ( 'NONE', #1406, #2047, #1356, .T. ) ;
#10227=FACE_OUTER_BOUND ( 'NONE', #10509, .T. ) ;
#10245=DIRECTION ( 'NONE',  ( 0.000000000000000000, 0.000000000000000000, -1.000000000000000000 ) ) ;
#10246=ORIENTED_EDGE ( 'NONE', *, *, #5469, .F. ) ;
#10271=DIRECTION ( 'NONE',  ( -0.000000000000000000, 0.8660254037844392627, 0.4999999999999990008 ) ) ;
#10273=LINE ( 'NONE', #875, #7893 ) ;
#10299=DIRECTION ( 'NONE',  ( 0.000000000000000000, 0.000000000000000000, 1.000000000000000000 ) ) ;
#10306=CARTESIAN_POINT ( 'NONE',  ( 2.000000000000000000, -1.329782007511007169, -0.7677499999999988223 ) ) ;
#10313=CARTESIAN_POINT ( 'NONE',  ( 2.000000000000000000, 0.000000000000000000, 0.000000000000000000 ) ) ;
#10314=ORIENTED_EDGE ( 'NONE', *, *, #3211, .T. ) ;
#10321=LINE ( 'NONE', #3377, #8780 ) ;
#10331=CARTESIAN_POINT ( 'NONE',  ( 2.000000000000000000, 1.773042676681340524, -2.059984127722458425E-15 ) ) ;
#10345=EDGE_CURVE ( 'NONE', #7434, #1907, #9137, .T. ) ;
#10346=DIRECTION ( 'NONE',  ( 0.000000000000000000, 0.000000000000000000, -1.000000000000000000 ) ) ;
#10353=ADVANCED_FACE ( 'NONE', ( #1569 ), #4969, .F. ) ;
#10355=EDGE_CURVE ( 'NONE', #4005, #3988, #6732, .T. ) ;
#10364=DIRECTION ( 'NONE',  ( 0.000000000000000000, 1.000000000000000000, -1.224646799147353207E-16 ) ) ;
#10407=PLANE ( 'NONE',  #2767 ) ;
#10416=SURFACE_STYLE_USAGE ( .BOTH. , #4482 ) ;
#10422=FACE_OUTER_BOUND ( 'NONE', #9223, .T. ) ;
#10432=UNCERTAINTY_MEASURE_WITH_UNIT (LENGTH_MEASURE( 1.000000000000000082E-05 ), #7554, 'distance_accuracy_value', 'NONE');
#10434=DIRECTION ( 'NONE',  ( 0.000000000000000000, 0.000000000000000000, 1.000000000000000000 ) ) ;
#10437=DIRECTION ( 'NONE',  ( -1.000000000000000000, -0.000000000000000000, -0.000000000000000000 ) ) ;
#10446=ORIENTED_EDGE ( 'NONE', *, *, #3221, .T. ) ;
#10456=VERTEX_POINT ( 'NONE', #1171 ) ;
#10463=CARTESIAN_POINT ( 'NONE',  ( 0.1999999999999987899, 0.000000000000000000, 0.000000000000000000 ) ) ;
#10470=CARTESIAN_POINT ( 'NONE',  ( 2.000000000000000000, 1.773042676681340524, -2.059984127722458425E-15 ) ) ;
#10503=CARTESIAN_POINT ( 'NONE',  ( 2.000000000000000000, 1.773042676681340524, -2.059984127722458425E-15 ) ) ;
#10509=EDGE_LOOP ( 'NONE', ( #8711, #715, #10559, #1279 ) ) ;
#10519=CIRCLE ( 'NONE', #5372, 3.500000000000000000 ) ;
#10540=DIRECTION ( 'NONE',  ( 0.000000000000000000, 0.000000000000000000, -1.000000000000000000 ) ) ;
#10543=CARTESIAN_POINT ( 'NONE',  ( 4.000000000000003553, 0.000000000000000000, 0.000000000000000000 ) ) ;
#10551=DIRECTION ( 'NONE',  ( 0.000000000000000000, 0.000000000000000000, -1.000000000000000000 ) ) ;
#10555=AXIS2_PLACEMENT_3D ( 'NONE', #7886, #3607, #368 ) ;
#10556=ORIENTED_EDGE ( 'NONE', *, *, #9478, .F. ) ;
#10559=ORIENTED_EDGE ( 'NONE', *, *, #7769, .T. ) ;
#10570=EDGE_CURVE ( 'NONE', #4079, #3725, #1197, .T. ) ;
#10572=DIRECTION ( 'NONE',  ( -1.000000000000000000, -0.000000000000000000, -0.000000000000000000 ) ) ;
#10573=CIRCLE ( 'NONE', #2235, 0.2000000000000000944 ) ;
#10574=FACE_OUTER_BOUND ( 'NONE', #8020, .T. ) ;
#10590=EDGE_CURVE ( 'NONE', #10667, #1487, #5293, .T. ) ;
#10625=EDGE_CURVE ( 'NONE', #1406, #3226, #9896, .T. ) ;
#10650=LINE ( 'NONE', #3039, #5426 ) ;
#10657=CARTESIAN_POINT ( 'NONE',  ( -31.74999999999995737, 0.000000000000000000, 0.000000000000000000 ) ) ;
#10660=FACE_OUTER_BOUND ( 'NONE', #3719, .T. ) ;
#10663=VERTEX_POINT ( 'NONE', #3018 ) ;
#10666=FACE_OUTER_BOUND ( 'NONE', #4068, .T. ) ;
#10667=VERTEX_POINT ( 'NONE', #4793 ) ;
#10677=DIRECTION ( 'NONE',  ( 0.000000000000000000, -0.8660254037844391517, -0.4999999999999991673 ) ) ;
#10685=FACE_OUTER_BOUND ( 'NONE', #5534, .T. ) ;
#10697=CARTESIAN_POINT ( 'NONE',  ( 0.000000000000000000, 0.8865213383406715941, 1.535499999999999199 ) ) ;
#10709=CARTESIAN_POINT ( 'NONE',  ( 0.1999999999999987899, 4.041334437186265510E-16, -3.299999999999999822 ) ) ;
#10716=VERTEX_POINT ( 'NONE', #4228 ) ;
#10726=ORIENTED_EDGE ( 'NONE', *, *, #9464, .T. ) ;
#10730=AXIS2_PLACEMENT_3D ( 'NONE', #549, #664, #5627 ) ;
#10734=ADVANCED_FACE ( 'NONE', ( #3391 ), #759, .T. ) ;
#10758=EDGE_CURVE ( 'NONE', #7385, #3226, #6172, .T. ) ;
#10774=EDGE_LOOP ( 'NONE', ( #9778, #5251, #4838, #216, #9667, #2157 ) ) ;
#10776=AXIS2_PLACEMENT_3D ( 'NONE', #1724, #2500, #7497 ) ;
#10789=EDGE_CURVE ( 'NONE', #7434, #7695, #9331, .T. ) ;
#10793=DIRECTION ( 'NONE',  ( 0.000000000000000000, -0.4999999999999991118, 0.8660254037844391517 ) ) ;
#10820=APPLICATION_CONTEXT ( 'automotive_design' ) ;
#10822=ADVANCED_FACE ( 'NONE', ( #3335 ), #2621, .F. ) ;
#10881=FILL_AREA_STYLE_COLOUR ( '', #10971 ) ;
#10890=CARTESIAN_POINT ( 'NONE',  ( 2.000000000000000000, -0.8865213383406694847, 1.535500000000001419 ) ) ;
#10891=PRODUCT_DEFINITION_CONTEXT ( 'detailed design', #2888, 'design' ) ;
#10899=DIRECTION ( 'NONE',  ( 0.000000000000000000, 0.000000000000000000, -1.000000000000000000 ) ) ;
#10906=EDGE_CURVE ( 'NONE', #10456, #3988, #3801, .T. ) ;
#10958=DIRECTION ( 'NONE',  ( 0.000000000000000000, 1.000000000000000000, -9.783878858594328898E-16 ) ) ;
#10966=FACE_OUTER_BOUND ( 'NONE', #2437, .T. ) ;
#10968=EDGE_CURVE ( 'NONE', #4272, #7462, #8806, .T. ) ;
#10971=COLOUR_RGB ( '', 0.31764706, 0.68627451, 0.89019608) ;
#10980=CARTESIAN_POINT ( 'NONE',  ( 2.000000000000000000, 2.065682573263594481E-15, 1.535500000000000309 ) ) ;
#10988=DIRECTION ( 'NONE',  ( -1.000000000000000000, -0.000000000000000000, -0.000000000000000000 ) ) ;
ENDSEC;
END-ISO-10303-21;
